ISO-10303-21;
HEADER;
/* Generated by software containing ST-Developer
 * from STEP Tools, Inc. (www.steptools.com) 
 */

FILE_DESCRIPTION(
/* description */ ('PAT-072'),
/* implementation_level */ '2;1');

FILE_NAME(
/* name */ 'M5x14 Cap Screw.step',
/* time_stamp */ '2026-10-29T20:11:56-07:00',
/* author */ (''),
/* organization */ (''),
/* preprocessor_version */ 'ST-DEVELOPER v20.2',
/* originating_system */ 'Autodesk Translation Framework v15.17.0.0',
/* authorisation */ '');

FILE_SCHEMA (('AUTOMOTIVE_DESIGN { 1 0 10303 214 3 1 1 }'));
ENDSEC;

DATA;
#10=MECHANICAL_DESIGN_GEOMETRIC_PRESENTATION_REPRESENTATION('',(#363),#11432);
#211=CONICAL_SURFACE('',#7106,0.4,0.785398163397448);
#212=CONICAL_SURFACE('',#7110,0.41,0.785398163397448);
#213=CONICAL_SURFACE('',#7114,0.26,0.463647609000806);
#220=ORIENTED_CLOSED_SHELL('',*,#6098,.F.);
#222=BREP_WITH_VOIDS('Body1',#6099,(#220));
#291=SHAPE_REPRESENTATION_RELATIONSHIP('SRR','None',#11595,#327);
#327=ADVANCED_BREP_SHAPE_REPRESENTATION('',(#222),#11426);
#363=STYLED_ITEM('',(#11826),#222);
#555=FACE_BOUND('',#1636,.T.);
#749=PLANE('',#7094);
#750=PLANE('',#7095);
#751=PLANE('',#7096);
#752=PLANE('',#7097);
#753=PLANE('',#7098);
#754=PLANE('',#7099);
#755=PLANE('',#7100);
#756=PLANE('',#7101);
#757=PLANE('',#7102);
#758=PLANE('',#7104);
#759=PLANE('',#7112);
#1097=FACE_OUTER_BOUND('',#1622,.T.);
#1098=FACE_OUTER_BOUND('',#1623,.T.);
#1099=FACE_OUTER_BOUND('',#1624,.T.);
#1100=FACE_OUTER_BOUND('',#1625,.T.);
#1101=FACE_OUTER_BOUND('',#1626,.T.);
#1102=FACE_OUTER_BOUND('',#1627,.T.);
#1103=FACE_OUTER_BOUND('',#1628,.T.);
#1104=FACE_OUTER_BOUND('',#1629,.T.);
#1105=FACE_OUTER_BOUND('',#1630,.T.);
#1106=FACE_OUTER_BOUND('',#1631,.T.);
#1107=FACE_OUTER_BOUND('',#1632,.T.);
#1108=FACE_OUTER_BOUND('',#1633,.T.);
#1109=FACE_OUTER_BOUND('',#1634,.T.);
#1110=FACE_OUTER_BOUND('',#1635,.T.);
#1111=FACE_OUTER_BOUND('',#1637,.T.);
#1112=FACE_OUTER_BOUND('',#1638,.T.);
#1622=EDGE_LOOP('',(#5288,#5289,#5290,#5291));
#1623=EDGE_LOOP('',(#5292,#5293,#5294,#5295));
#1624=EDGE_LOOP('',(#5296,#5297,#5298,#5299));
#1625=EDGE_LOOP('',(#5300,#5301,#5302,#5303));
#1626=EDGE_LOOP('',(#5304,#5305,#5306,#5307));
#1627=EDGE_LOOP('',(#5308,#5309,#5310,#5311));
#1628=EDGE_LOOP('',(#5312,#5313,#5314,#5315,#5316,#5317));
#1629=EDGE_LOOP('',(#5318,#5319,#5320,#5321,#5322,#5323));
#1630=EDGE_LOOP('',(#5324));
#1631=EDGE_LOOP('',(#5325));
#1632=EDGE_LOOP('',(#5326,#5327,#5328,#5329));
#1633=EDGE_LOOP('',(#5330,#5331,#5332,#5333));
#1634=EDGE_LOOP('',(#5334,#5335,#5336,#5337));
#1635=EDGE_LOOP('',(#5338));
#1636=EDGE_LOOP('',(#5339));
#1637=EDGE_LOOP('',(#5340,#5341,#5342,#5343));
#1638=EDGE_LOOP('',(#5344,#5345,#5346,#5347));
#2031=LINE('',#11010,#2450);
#2032=LINE('',#11012,#2451);
#2033=LINE('',#11014,#2452);
#2034=LINE('',#11015,#2453);
#2035=LINE('',#11018,#2454);
#2036=LINE('',#11020,#2455);
#2037=LINE('',#11021,#2456);
#2038=LINE('',#11024,#2457);
#2039=LINE('',#11026,#2458);
#2040=LINE('',#11027,#2459);
#2041=LINE('',#11030,#2460);
#2042=LINE('',#11032,#2461);
#2043=LINE('',#11033,#2462);
#2044=LINE('',#11036,#2463);
#2045=LINE('',#11038,#2464);
#2046=LINE('',#11039,#2465);
#2047=LINE('',#11041,#2466);
#2048=LINE('',#11042,#2467);
#2049=LINE('',#11054,#2468);
#2050=LINE('',#11058,#2469);
#2051=LINE('',#11062,#2470);
#2052=LINE('',#11069,#2471);
#2053=LINE('',#11071,#2472);
#2450=VECTOR('',#8768,1.);
#2451=VECTOR('',#8769,1.);
#2452=VECTOR('',#8770,1.);
#2453=VECTOR('',#8771,1.);
#2454=VECTOR('',#8774,1.);
#2455=VECTOR('',#8775,1.);
#2456=VECTOR('',#8776,1.);
#2457=VECTOR('',#8779,1.);
#2458=VECTOR('',#8780,1.);
#2459=VECTOR('',#8781,1.);
#2460=VECTOR('',#8784,1.);
#2461=VECTOR('',#8785,1.);
#2462=VECTOR('',#8786,1.);
#2463=VECTOR('',#8789,1.);
#2464=VECTOR('',#8790,1.);
#2465=VECTOR('',#8791,1.);
#2466=VECTOR('',#8794,1.);
#2467=VECTOR('',#8795,1.);
#2468=VECTOR('',#8812,0.4);
#2469=VECTOR('',#8817,0.425);
#2470=VECTOR('',#8822,0.41);
#2471=VECTOR('',#8831,0.26);
#2472=VECTOR('',#8834,0.25);
#2797=CIRCLE('',#7103,0.24505);
#2798=CIRCLE('',#7105,0.375);
#2799=CIRCLE('',#7107,0.425);
#2800=CIRCLE('',#7109,0.425);
#2801=CIRCLE('',#7111,0.395);
#2802=CIRCLE('',#7113,0.27);
#2803=CIRCLE('',#7115,0.24505);
#3236=VERTEX_POINT('',#11008);
#3237=VERTEX_POINT('',#11009);
#3238=VERTEX_POINT('',#11011);
#3239=VERTEX_POINT('',#11013);
#3240=VERTEX_POINT('',#11017);
#3241=VERTEX_POINT('',#11019);
#3242=VERTEX_POINT('',#11023);
#3243=VERTEX_POINT('',#11025);
#3244=VERTEX_POINT('',#11029);
#3245=VERTEX_POINT('',#11031);
#3246=VERTEX_POINT('',#11035);
#3247=VERTEX_POINT('',#11037);
#3248=VERTEX_POINT('',#11046);
#3249=VERTEX_POINT('',#11049);
#3250=VERTEX_POINT('',#11052);
#3251=VERTEX_POINT('',#11056);
#3252=VERTEX_POINT('',#11060);
#3253=VERTEX_POINT('',#11064);
#3254=VERTEX_POINT('',#11067);
#3933=EDGE_CURVE('',#3236,#3237,#2031,.T.);
#3934=EDGE_CURVE('',#3237,#3238,#2032,.T.);
#3935=EDGE_CURVE('',#3238,#3239,#2033,.T.);
#3936=EDGE_CURVE('',#3236,#3239,#2034,.T.);
#3937=EDGE_CURVE('',#3237,#3240,#2035,.T.);
#3938=EDGE_CURVE('',#3240,#3241,#2036,.T.);
#3939=EDGE_CURVE('',#3241,#3238,#2037,.T.);
#3940=EDGE_CURVE('',#3240,#3242,#2038,.T.);
#3941=EDGE_CURVE('',#3242,#3243,#2039,.T.);
#3942=EDGE_CURVE('',#3243,#3241,#2040,.T.);
#3943=EDGE_CURVE('',#3242,#3244,#2041,.T.);
#3944=EDGE_CURVE('',#3244,#3245,#2042,.T.);
#3945=EDGE_CURVE('',#3245,#3243,#2043,.T.);
#3946=EDGE_CURVE('',#3244,#3246,#2044,.T.);
#3947=EDGE_CURVE('',#3246,#3247,#2045,.T.);
#3948=EDGE_CURVE('',#3247,#3245,#2046,.T.);
#3949=EDGE_CURVE('',#3246,#3236,#2047,.T.);
#3950=EDGE_CURVE('',#3239,#3247,#2048,.T.);
#3951=EDGE_CURVE('',#3248,#3248,#2797,.T.);
#3952=EDGE_CURVE('',#3249,#3249,#2798,.T.);
#3953=EDGE_CURVE('',#3250,#3250,#2799,.T.);
#3954=EDGE_CURVE('',#3250,#3249,#2049,.T.);
#3955=EDGE_CURVE('',#3251,#3251,#2800,.T.);
#3956=EDGE_CURVE('',#3251,#3250,#2050,.T.);
#3957=EDGE_CURVE('',#3252,#3252,#2801,.T.);
#3958=EDGE_CURVE('',#3252,#3251,#2051,.T.);
#3959=EDGE_CURVE('',#3253,#3253,#2802,.T.);
#3960=EDGE_CURVE('',#3254,#3254,#2803,.F.);
#3961=EDGE_CURVE('',#3254,#3253,#2052,.T.);
#3962=EDGE_CURVE('',#3248,#3254,#2053,.T.);
#5288=ORIENTED_EDGE('',*,*,#3933,.T.);
#5289=ORIENTED_EDGE('',*,*,#3934,.T.);
#5290=ORIENTED_EDGE('',*,*,#3935,.T.);
#5291=ORIENTED_EDGE('',*,*,#3936,.F.);
#5292=ORIENTED_EDGE('',*,*,#3937,.T.);
#5293=ORIENTED_EDGE('',*,*,#3938,.T.);
#5294=ORIENTED_EDGE('',*,*,#3939,.T.);
#5295=ORIENTED_EDGE('',*,*,#3934,.F.);
#5296=ORIENTED_EDGE('',*,*,#3940,.T.);
#5297=ORIENTED_EDGE('',*,*,#3941,.T.);
#5298=ORIENTED_EDGE('',*,*,#3942,.T.);
#5299=ORIENTED_EDGE('',*,*,#3938,.F.);
#5300=ORIENTED_EDGE('',*,*,#3943,.T.);
#5301=ORIENTED_EDGE('',*,*,#3944,.T.);
#5302=ORIENTED_EDGE('',*,*,#3945,.T.);
#5303=ORIENTED_EDGE('',*,*,#3941,.F.);
#5304=ORIENTED_EDGE('',*,*,#3946,.T.);
#5305=ORIENTED_EDGE('',*,*,#3947,.T.);
#5306=ORIENTED_EDGE('',*,*,#3948,.T.);
#5307=ORIENTED_EDGE('',*,*,#3944,.F.);
#5308=ORIENTED_EDGE('',*,*,#3949,.T.);
#5309=ORIENTED_EDGE('',*,*,#3936,.T.);
#5310=ORIENTED_EDGE('',*,*,#3950,.T.);
#5311=ORIENTED_EDGE('',*,*,#3947,.F.);
#5312=ORIENTED_EDGE('',*,*,#3949,.F.);
#5313=ORIENTED_EDGE('',*,*,#3946,.F.);
#5314=ORIENTED_EDGE('',*,*,#3943,.F.);
#5315=ORIENTED_EDGE('',*,*,#3940,.F.);
#5316=ORIENTED_EDGE('',*,*,#3937,.F.);
#5317=ORIENTED_EDGE('',*,*,#3933,.F.);
#5318=ORIENTED_EDGE('',*,*,#3950,.F.);
#5319=ORIENTED_EDGE('',*,*,#3935,.F.);
#5320=ORIENTED_EDGE('',*,*,#3939,.F.);
#5321=ORIENTED_EDGE('',*,*,#3942,.F.);
#5322=ORIENTED_EDGE('',*,*,#3945,.F.);
#5323=ORIENTED_EDGE('',*,*,#3948,.F.);
#5324=ORIENTED_EDGE('',*,*,#3951,.F.);
#5325=ORIENTED_EDGE('',*,*,#3952,.F.);
#5326=ORIENTED_EDGE('',*,*,#3953,.F.);
#5327=ORIENTED_EDGE('',*,*,#3954,.T.);
#5328=ORIENTED_EDGE('',*,*,#3952,.T.);
#5329=ORIENTED_EDGE('',*,*,#3954,.F.);
#5330=ORIENTED_EDGE('',*,*,#3955,.F.);
#5331=ORIENTED_EDGE('',*,*,#3956,.T.);
#5332=ORIENTED_EDGE('',*,*,#3953,.T.);
#5333=ORIENTED_EDGE('',*,*,#3956,.F.);
#5334=ORIENTED_EDGE('',*,*,#3957,.F.);
#5335=ORIENTED_EDGE('',*,*,#3958,.T.);
#5336=ORIENTED_EDGE('',*,*,#3955,.T.);
#5337=ORIENTED_EDGE('',*,*,#3958,.F.);
#5338=ORIENTED_EDGE('',*,*,#3957,.T.);
#5339=ORIENTED_EDGE('',*,*,#3959,.F.);
#5340=ORIENTED_EDGE('',*,*,#3960,.F.);
#5341=ORIENTED_EDGE('',*,*,#3961,.T.);
#5342=ORIENTED_EDGE('',*,*,#3959,.T.);
#5343=ORIENTED_EDGE('',*,*,#3961,.F.);
#5344=ORIENTED_EDGE('',*,*,#3951,.T.);
#5345=ORIENTED_EDGE('',*,*,#3962,.T.);
#5346=ORIENTED_EDGE('',*,*,#3960,.T.);
#5347=ORIENTED_EDGE('',*,*,#3962,.F.);
#5680=CYLINDRICAL_SURFACE('',#7108,0.425);
#5681=CYLINDRICAL_SURFACE('',#7116,0.24505);
#5996=ADVANCED_FACE('',(#1097),#749,.F.);
#5997=ADVANCED_FACE('',(#1098),#750,.F.);
#5998=ADVANCED_FACE('',(#1099),#751,.F.);
#5999=ADVANCED_FACE('',(#1100),#752,.F.);
#6000=ADVANCED_FACE('',(#1101),#753,.F.);
#6001=ADVANCED_FACE('',(#1102),#754,.F.);
#6002=ADVANCED_FACE('',(#1103),#755,.F.);
#6003=ADVANCED_FACE('',(#1104),#756,.F.);
#6004=ADVANCED_FACE('',(#1105),#757,.F.);
#6005=ADVANCED_FACE('',(#1106),#758,.T.);
#6006=ADVANCED_FACE('',(#1107),#211,.T.);
#6007=ADVANCED_FACE('',(#1108),#5680,.T.);
#6008=ADVANCED_FACE('',(#1109),#212,.T.);
#6009=ADVANCED_FACE('',(#1110,#555),#759,.T.);
#6010=ADVANCED_FACE('',(#1111),#213,.T.);
#6011=ADVANCED_FACE('',(#1112),#5681,.T.);
#6098=CLOSED_SHELL('',(#5996,#5997,#5998,#5999,#6000,#6001,#6002,#6003));
#6099=CLOSED_SHELL('',(#6004,#6005,#6006,#6007,#6008,#6009,#6010,#6011));
#7093=AXIS2_PLACEMENT_3D('',#11006,#8764,#8765);
#7094=AXIS2_PLACEMENT_3D('',#11007,#8766,#8767);
#7095=AXIS2_PLACEMENT_3D('',#11016,#8772,#8773);
#7096=AXIS2_PLACEMENT_3D('',#11022,#8777,#8778);
#7097=AXIS2_PLACEMENT_3D('',#11028,#8782,#8783);
#7098=AXIS2_PLACEMENT_3D('',#11034,#8787,#8788);
#7099=AXIS2_PLACEMENT_3D('',#11040,#8792,#8793);
#7100=AXIS2_PLACEMENT_3D('',#11043,#8796,#8797);
#7101=AXIS2_PLACEMENT_3D('',#11044,#8798,#8799);
#7102=AXIS2_PLACEMENT_3D('',#11045,#8800,#8801);
#7103=AXIS2_PLACEMENT_3D('',#11047,#8802,#8803);
#7104=AXIS2_PLACEMENT_3D('',#11048,#8804,#8805);
#7105=AXIS2_PLACEMENT_3D('',#11050,#8806,#8807);
#7106=AXIS2_PLACEMENT_3D('',#11051,#8808,#8809);
#7107=AXIS2_PLACEMENT_3D('',#11053,#8810,#8811);
#7108=AXIS2_PLACEMENT_3D('',#11055,#8813,#8814);
#7109=AXIS2_PLACEMENT_3D('',#11057,#8815,#8816);
#7110=AXIS2_PLACEMENT_3D('',#11059,#8818,#8819);
#7111=AXIS2_PLACEMENT_3D('',#11061,#8820,#8821);
#7112=AXIS2_PLACEMENT_3D('',#11063,#8823,#8824);
#7113=AXIS2_PLACEMENT_3D('',#11065,#8825,#8826);
#7114=AXIS2_PLACEMENT_3D('',#11066,#8827,#8828);
#7115=AXIS2_PLACEMENT_3D('',#11068,#8829,#8830);
#7116=AXIS2_PLACEMENT_3D('',#11070,#8832,#8833);
#8764=DIRECTION('axis',(0.,0.,1.));
#8765=DIRECTION('refdir',(1.,0.,0.));
#8766=DIRECTION('center_axis',(0.866025403784439,0.,-0.5));
#8767=DIRECTION('ref_axis',(0.5,0.,0.866025403784439));
#8768=DIRECTION('',(-0.5,0.,-0.866025403784439));
#8769=DIRECTION('',(0.,-1.,0.));
#8770=DIRECTION('',(0.5,0.,0.866025403784439));
#8771=DIRECTION('',(0.,-1.,0.));
#8772=DIRECTION('center_axis',(1.20185167898973E-16,0.,-1.));
#8773=DIRECTION('ref_axis',(1.,0.,1.20185167898973E-16));
#8774=DIRECTION('',(-1.,0.,-1.20185167898973E-16));
#8775=DIRECTION('',(0.,-1.,0.));
#8776=DIRECTION('',(1.,0.,1.20185167898973E-16));
#8777=DIRECTION('center_axis',(-0.866025403784439,0.,-0.5));
#8778=DIRECTION('ref_axis',(0.5,0.,-0.866025403784439));
#8779=DIRECTION('',(-0.5,0.,0.866025403784439));
#8780=DIRECTION('',(0.,-1.,0.));
#8781=DIRECTION('',(0.5,0.,-0.866025403784439));
#8782=DIRECTION('center_axis',(-0.866025403784439,0.,0.5));
#8783=DIRECTION('ref_axis',(-0.5,0.,-0.866025403784439));
#8784=DIRECTION('',(0.5,0.,0.866025403784439));
#8785=DIRECTION('',(0.,-1.,0.));
#8786=DIRECTION('',(-0.5,0.,-0.866025403784439));
#8787=DIRECTION('center_axis',(-2.40370335797945E-16,0.,1.));
#8788=DIRECTION('ref_axis',(-1.,0.,-2.40370335797945E-16));
#8789=DIRECTION('',(1.,0.,2.40370335797945E-16));
#8790=DIRECTION('',(0.,-1.,0.));
#8791=DIRECTION('',(-1.,0.,-2.40370335797945E-16));
#8792=DIRECTION('center_axis',(0.866025403784439,0.,0.5));
#8793=DIRECTION('ref_axis',(-0.5,0.,0.866025403784439));
#8794=DIRECTION('',(0.5,0.,-0.866025403784439));
#8795=DIRECTION('',(-0.5,0.,0.866025403784439));
#8796=DIRECTION('center_axis',(0.,1.,0.));
#8797=DIRECTION('ref_axis',(1.,0.,0.));
#8798=DIRECTION('center_axis',(0.,-1.,0.));
#8799=DIRECTION('ref_axis',(0.,0.,-1.));
#8800=DIRECTION('center_axis',(0.,1.,0.));
#8801=DIRECTION('ref_axis',(1.,0.,0.));
#8802=DIRECTION('center_axis',(0.,1.,0.));
#8803=DIRECTION('ref_axis',(1.,0.,0.));
#8804=DIRECTION('center_axis',(0.,1.,0.));
#8805=DIRECTION('ref_axis',(0.,0.,1.));
#8806=DIRECTION('center_axis',(0.,-1.,0.));
#8807=DIRECTION('ref_axis',(1.,0.,0.));
#8808=DIRECTION('center_axis',(0.,-1.,0.));
#8809=DIRECTION('ref_axis',(1.,0.,0.));
#8810=DIRECTION('center_axis',(0.,-1.,0.));
#8811=DIRECTION('ref_axis',(1.,0.,0.));
#8812=DIRECTION('',(0.707106781186548,0.707106781186547,8.65956056235493E-17));
#8813=DIRECTION('center_axis',(0.,-1.,0.));
#8814=DIRECTION('ref_axis',(1.,0.,0.));
#8815=DIRECTION('center_axis',(0.,-1.,0.));
#8816=DIRECTION('ref_axis',(1.,0.,0.));
#8817=DIRECTION('',(0.,1.,0.));
#8818=DIRECTION('center_axis',(0.,1.,0.));
#8819=DIRECTION('ref_axis',(1.,0.,0.));
#8820=DIRECTION('center_axis',(0.,-1.,0.));
#8821=DIRECTION('ref_axis',(1.,0.,0.));
#8822=DIRECTION('',(-0.707106781186547,0.707106781186548,-8.65956056235493E-17));
#8823=DIRECTION('center_axis',(0.,-1.,0.));
#8824=DIRECTION('ref_axis',(0.,0.,-1.));
#8825=DIRECTION('center_axis',(0.,-1.,0.));
#8826=DIRECTION('ref_axis',(1.,0.,0.));
#8827=DIRECTION('center_axis',(0.,1.,0.));
#8828=DIRECTION('ref_axis',(1.,0.,0.));
#8829=DIRECTION('center_axis',(0.,1.,0.));
#8830=DIRECTION('ref_axis',(1.,0.,0.));
#8831=DIRECTION('',(-0.447213595499958,0.894427190999916,-5.47678698264203E-17));
#8832=DIRECTION('center_axis',(0.,-1.,0.));
#8833=DIRECTION('ref_axis',(1.,0.,0.));
#8834=DIRECTION('',(0.,1.,0.));
#11006=CARTESIAN_POINT('',(0.,0.,0.));
#11007=CARTESIAN_POINT('Origin',(0.115470053837925,-0.5,-0.2));
#11008=CARTESIAN_POINT('',(0.23094010767585,-0.5,0.));
#11009=CARTESIAN_POINT('',(0.115470053837925,-0.5,-0.2));
#11010=CARTESIAN_POINT('',(0.23094010767585,-0.5,0.));
#11011=CARTESIAN_POINT('',(0.115470053837925,-0.8,-0.2));
#11012=CARTESIAN_POINT('',(0.115470053837925,-0.5,-0.2));
#11013=CARTESIAN_POINT('',(0.23094010767585,-0.8,0.));
#11014=CARTESIAN_POINT('',(0.23094010767585,-0.8,0.));
#11015=CARTESIAN_POINT('',(0.23094010767585,-0.5,0.));
#11016=CARTESIAN_POINT('Origin',(-0.115470053837925,-0.5,-0.2));
#11017=CARTESIAN_POINT('',(-0.115470053837925,-0.5,-0.2));
#11018=CARTESIAN_POINT('',(0.115470053837925,-0.5,-0.2));
#11019=CARTESIAN_POINT('',(-0.115470053837925,-0.8,-0.2));
#11020=CARTESIAN_POINT('',(-0.115470053837925,-0.5,-0.2));
#11021=CARTESIAN_POINT('',(0.115470053837925,-0.8,-0.2));
#11022=CARTESIAN_POINT('Origin',(-0.23094010767585,-0.5,-2.77555756156289E-17));
#11023=CARTESIAN_POINT('',(-0.23094010767585,-0.5,-2.82820063659975E-17));
#11024=CARTESIAN_POINT('',(-0.115470053837925,-0.5,-0.2));
#11025=CARTESIAN_POINT('',(-0.23094010767585,-0.8,-2.77555756156289E-17));
#11026=CARTESIAN_POINT('',(-0.23094010767585,-0.5,-2.82820063659975E-17));
#11027=CARTESIAN_POINT('',(-0.115470053837925,-0.8,-0.2));
#11028=CARTESIAN_POINT('Origin',(-0.115470053837925,-0.5,0.2));
#11029=CARTESIAN_POINT('',(-0.115470053837925,-0.5,0.2));
#11030=CARTESIAN_POINT('',(-0.23094010767585,-0.5,-2.82820063659975E-17));
#11031=CARTESIAN_POINT('',(-0.115470053837925,-0.8,0.2));
#11032=CARTESIAN_POINT('',(-0.115470053837925,-0.5,0.2));
#11033=CARTESIAN_POINT('',(-0.23094010767585,-0.8,-2.82820063659975E-17));
#11034=CARTESIAN_POINT('Origin',(0.115470053837925,-0.5,0.2));
#11035=CARTESIAN_POINT('',(0.115470053837925,-0.5,0.2));
#11036=CARTESIAN_POINT('',(-0.115470053837925,-0.5,0.2));
#11037=CARTESIAN_POINT('',(0.115470053837925,-0.8,0.2));
#11038=CARTESIAN_POINT('',(0.115470053837925,-0.5,0.2));
#11039=CARTESIAN_POINT('',(-0.115470053837925,-0.8,0.2));
#11040=CARTESIAN_POINT('Origin',(0.23094010767585,-0.5,0.));
#11041=CARTESIAN_POINT('',(0.115470053837925,-0.5,0.2));
#11042=CARTESIAN_POINT('',(0.115470053837925,-0.8,0.2));
#11043=CARTESIAN_POINT('Origin',(0.,-0.5,0.));
#11044=CARTESIAN_POINT('Origin',(0.,-0.8,0.));
#11045=CARTESIAN_POINT('Origin',(0.,-1.4,0.));
#11046=CARTESIAN_POINT('',(-0.24505,-1.4,3.00099698131059E-17));
#11047=CARTESIAN_POINT('Origin',(0.,-1.4,0.));
#11048=CARTESIAN_POINT('Origin',(0.375,0.5,0.));
#11049=CARTESIAN_POINT('',(-0.375,0.5,-4.59242549680257E-17));
#11050=CARTESIAN_POINT('Origin',(0.,0.5,0.));
#11051=CARTESIAN_POINT('Origin',(0.,0.475,0.));
#11052=CARTESIAN_POINT('',(-0.425,0.45,-5.20474889637625E-17));
#11053=CARTESIAN_POINT('Origin',(0.,0.45,0.));
#11054=CARTESIAN_POINT('',(-0.4,0.475,-4.89858719658941E-17));
#11055=CARTESIAN_POINT('Origin',(0.,0.24,0.));
#11056=CARTESIAN_POINT('',(-0.425,0.0299999999999998,-5.20474889637625E-17));
#11057=CARTESIAN_POINT('Origin',(0.,0.0299999999999998,0.));
#11058=CARTESIAN_POINT('',(-0.425,0.24,-5.20474889637625E-17));
#11059=CARTESIAN_POINT('Origin',(0.,0.0150000000000001,0.));
#11060=CARTESIAN_POINT('',(-0.395,4.85722573273506E-17,-4.83735485663204E-17));
#11061=CARTESIAN_POINT('Origin',(0.,0.,0.));
#11062=CARTESIAN_POINT('',(-0.41,0.0150000000000001,-5.02105187650415E-17));
#11063=CARTESIAN_POINT('Origin',(0.27,0.,0.));
#11064=CARTESIAN_POINT('',(-0.27,0.,-3.30654635769785E-17));
#11065=CARTESIAN_POINT('Origin',(0.,0.,0.));
#11066=CARTESIAN_POINT('Origin',(0.,-0.02,0.));
#11067=CARTESIAN_POINT('',(-0.24505,-0.0498999999999999,3.00099698131059E-17));
#11068=CARTESIAN_POINT('Origin',(0.,-0.0498999999999999,0.));
#11069=CARTESIAN_POINT('',(-0.26,-0.02,-3.18408167778312E-17));
#11070=CARTESIAN_POINT('Origin',(0.,-0.995,0.));
#11071=CARTESIAN_POINT('',(-0.24505,-0.995,-3.00099698131059E-17));
#11387=UNCERTAINTY_MEASURE_WITH_UNIT(LENGTH_MEASURE(0.001),#11433,
'DISTANCE_ACCURACY_VALUE',
'Maximum model space distance between geometric entities at asserted c
onnectivities');
#11393=UNCERTAINTY_MEASURE_WITH_UNIT(LENGTH_MEASURE(0.001),#11433,
'DISTANCE_ACCURACY_VALUE',
'Maximum model space distance between geometric entities at asserted c
onnectivities');
#11426=(
GEOMETRIC_REPRESENTATION_CONTEXT(3)
GLOBAL_UNCERTAINTY_ASSIGNED_CONTEXT((#11387))
GLOBAL_UNIT_ASSIGNED_CONTEXT((#11433,#11435,#11436))
REPRESENTATION_CONTEXT('','3D')
);
#11432=(
GEOMETRIC_REPRESENTATION_CONTEXT(3)
GLOBAL_UNCERTAINTY_ASSIGNED_CONTEXT((#11393))
GLOBAL_UNIT_ASSIGNED_CONTEXT((#11433,#11435,#11436))
REPRESENTATION_CONTEXT('','3D')
);
#11433=(
LENGTH_UNIT()
NAMED_UNIT(*)
SI_UNIT(.CENTI.,.METRE.)
);
#11435=(
NAMED_UNIT(*)
PLANE_ANGLE_UNIT()
SI_UNIT($,.RADIAN.)
);
#11436=(
NAMED_UNIT(*)
SI_UNIT($,.STERADIAN.)
SOLID_ANGLE_UNIT()
);
#11469=SHAPE_DEFINITION_REPRESENTATION(#11507,#11595);
#11507=PRODUCT_DEFINITION_SHAPE('',$,#11634);
#11595=SHAPE_REPRESENTATION('',(#7093),#11426);
#11601=PRODUCT_DEFINITION_CONTEXT('part definition',#11717,'design');
#11634=PRODUCT_DEFINITION('M5x14 Cap Screw','M5x14 Cap Screw',
#11672,#11601);
#11672=PRODUCT_DEFINITION_FORMATION('',$,#11751);
#11717=APPLICATION_CONTEXT(
'Core Data for Automotive Mechanical Design Process');
#11718=PRODUCT_CONTEXT('part definition',#11717,'mechanical');
#11751=PRODUCT('M5x14 Cap Screw','M5x14 Cap Screw',
'M5x14 Cap Screw',(#11718));
#11820=COLOUR_RGB('Black',0.12,0.14,0.17);
#11821=FILL_AREA_STYLE_COLOUR('',#11820);
#11822=FILL_AREA_STYLE('',(#11821));
#11823=SURFACE_STYLE_FILL_AREA(#11822);
#11824=SURFACE_SIDE_STYLE('',(#11823));
#11825=SURFACE_STYLE_USAGE(.BOTH.,#11824);
#11826=PRESENTATION_STYLE_ASSIGNMENT((#11825));
ENDSEC;
END-ISO-10303-21;
